ISO-10303-21;
HEADER;
FILE_DESCRIPTION (('STEP AP214'),
    '1' );
FILE_NAME ('Rotor.step',
    '2026-10-24T11:32:06',
    ( '' ),
    ( '' ),
    'SwSTEP 2.0',
    'SolidWorks 2025',
    '' );
FILE_SCHEMA (( 'AUTOMOTIVE_DESIGN' ));
ENDSEC;

DATA;
#28=LINE ( 'NONE', #15774, #16810 ) ;
#37=ORIENTED_EDGE ( 'NONE', *, *, #50660, .F. ) ;
#113=EDGE_CURVE ( 'NONE', #26527, #41000, #12273, .T. ) ;
#151=CARTESIAN_POINT ( 'NONE',  ( -0.2480359799030329715, -0.6299212598425202314, 0.2799391584775194342 ) ) ;
#198=VECTOR ( 'NONE', #32810, 39.37007874015748854 ) ;
#275=( NAMED_UNIT ( * ) PLANE_ANGLE_UNIT ( ) SI_UNIT ( $, .RADIAN. ) );
#286=VERTEX_POINT ( 'NONE', #38322 ) ;
#426=DIRECTION ( 'NONE',  ( -0.9465353838348410376, -0.000000000000000000, -0.3226000110797114795 ) ) ;
#431=CIRCLE ( 'NONE', #50675, 0.3740157480314960647 ) ;
#501=ADVANCED_FACE ( 'NONE', ( #36470 ), #20194, .F. ) ;
#516=DIRECTION ( 'NONE',  ( 0.000000000000000000, 1.000000000000000000, 0.000000000000000000 ) ) ;
#517=FACE_OUTER_BOUND ( 'NONE', #33825, .T. ) ;
#547=AXIS2_PLACEMENT_3D ( 'NONE', #36809, #1941, #6065 ) ;
#553=DIRECTION ( 'NONE',  ( -0.000000000000000000, 1.000000000000000000, -0.000000000000000000 ) ) ;
#604=ORIENTED_EDGE ( 'NONE', *, *, #14891, .T. ) ;
#693=AXIS2_PLACEMENT_3D ( 'NONE', #4212, #47029, #7581 ) ;
#720=AXIS2_PLACEMENT_3D ( 'NONE', #26978, #18743, #30872 ) ;
#789=PLANE ( 'NONE',  #29930 ) ;
#832=ORIENTED_EDGE ( 'NONE', *, *, #47602, .F. ) ;
#833=EDGE_CURVE ( 'NONE', #33133, #25081, #27366, .T. ) ;
#942=LINE ( 'NONE', #20035, #38229 ) ;
#945=VERTEX_POINT ( 'NONE', #32805 ) ;
#976=EDGE_LOOP ( 'NONE', ( #38466, #49950, #28747, #13635, #8159, #50892, #23802 ) ) ;
#985=CIRCLE ( 'NONE', #47931, 0.3740157480314960647 ) ;
#1035=CARTESIAN_POINT ( 'NONE',  ( -0.4371342596750092402, 2.755905511811024056, -1.309652049997256373 ) ) ;
#1282=AXIS2_PLACEMENT_3D ( 'NONE', #10730, #26466, #26719 ) ;
#1320=AXIS2_PLACEMENT_3D ( 'NONE', #11866, #19853, #35621 ) ;
#1378=ORIENTED_EDGE ( 'NONE', *, *, #44567, .T. ) ;
#1477=AXIS2_PLACEMENT_3D ( 'NONE', #14187, #37188, #5686 ) ;
#1528=VERTEX_POINT ( 'NONE', #30068 ) ;
#1593=EDGE_CURVE ( 'NONE', #20677, #16212, #43533, .T. ) ;
#1594=EDGE_LOOP ( 'NONE', ( #7957, #25281, #38663, #22736 ) ) ;
#1646=DIRECTION ( 'NONE',  ( 0.000000000000000000, -1.000000000000000000, 0.000000000000000000 ) ) ;
#1875=CIRCLE ( 'NONE', #24952, 0.3740157480314960647 ) ;
#1941=DIRECTION ( 'NONE',  ( 0.000000000000000000, -1.000000000000000000, 0.000000000000000000 ) ) ;
#1964=CARTESIAN_POINT ( 'NONE',  ( 1.157218145390799036, 0.000000000000000000, 0.2363238328731523952 ) ) ;
#2021=EDGE_CURVE ( 'NONE', #22341, #945, #27831, .T. ) ;
#2224=AXIS2_PLACEMENT_3D ( 'NONE', #2386, #14251, #45723 ) ;
#2293=DIRECTION ( 'NONE',  ( 0.000000000000000000, 0.000000000000000000, -1.000000000000000000 ) ) ;
#2386=CARTESIAN_POINT ( 'NONE',  ( 0.000000000000000000, 2.755905511811022723, 0.000000000000000000 ) ) ;
#2391=ORIENTED_EDGE ( 'NONE', *, *, #41956, .T. ) ;
#2447=DIRECTION ( 'NONE',  ( 0.000000000000000000, 0.000000000000000000, -1.000000000000000000 ) ) ;
#2585=AXIS2_PLACEMENT_3D ( 'NONE', #7748, #39243, #3883 ) ;
#2595=EDGE_CURVE ( 'NONE', #286, #37788, #39416, .T. ) ;
#2700=AXIS2_PLACEMENT_3D ( 'NONE', #21274, #1646, #17399 ) ;
#2736=VERTEX_POINT ( 'NONE', #50238 ) ;
#2797=DIRECTION ( 'NONE',  ( 0.000000000000000000, -1.000000000000000000, 0.000000000000000000 ) ) ;
#2826=CARTESIAN_POINT ( 'NONE',  ( -0.9156248155784967313, 2.755905511811024056, 1.033395398741681293 ) ) ;
#2901=DIRECTION ( 'NONE',  ( -0.8439299085898972486, 0.000000000000000000, 0.5364534550056021533 ) ) ;
#2958=AXIS2_PLACEMENT_3D ( 'NONE', #50068, #46952, #14751 ) ;
#3073=ORIENTED_EDGE ( 'NONE', *, *, #49878, .T. ) ;
#3112=AXIS2_PLACEMENT_3D ( 'NONE', #36008, #15857, #27226 ) ;
#3129=ORIENTED_EDGE ( 'NONE', *, *, #42959, .T. ) ;
#3147=CARTESIAN_POINT ( 'NONE',  ( 0.000000000000000000, 2.755905511811024056, -1.181102362204723200 ) ) ;
#3166=ADVANCED_FACE ( 'NONE', ( #49432 ), #34246, .T. ) ;
#3236=DIRECTION ( 'NONE',  ( -0.000000000000000000, -1.000000000000000000, -0.000000000000000000 ) ) ;
#3286=DIRECTION ( 'NONE',  ( 0.000000000000000000, -1.000000000000000000, -0.000000000000000000 ) ) ;
#3571=VECTOR ( 'NONE', #5429, 39.37007874015748143 ) ;
#3592=CARTESIAN_POINT ( 'NONE',  ( -0.2834077913992259501, 2.755905511811024056, -0.2440651625074179987 ) ) ;
#3710=ADVANCED_FACE ( 'NONE', ( #8320 ), #4445, .T. ) ;
#3783=FACE_OUTER_BOUND ( 'NONE', #42562, .T. ) ;
#3883=DIRECTION ( 'NONE',  ( 0.1938878870612536220, 0.000000000000000000, 0.9810236935216818388 ) ) ;
#3918=CARTESIAN_POINT ( 'NONE',  ( -0.3739466299075467348, 0.000000000000000000, -1.120342228065320134 ) ) ;
#3968=CARTESIAN_POINT ( 'NONE',  ( -1.004926760980926481, 2.755905511811024056, -0.6205843980233154422 ) ) ;
#4085=ORIENTED_EDGE ( 'NONE', *, *, #19872, .T. ) ;
#4113=CARTESIAN_POINT ( 'NONE',  ( 0.3530705266098149164, 2.755905511811024056, -0.1234057657284599735 ) ) ;
#4137=CARTESIAN_POINT ( 'NONE',  ( 0.000000000000000000, 2.755905511811024056, 0.000000000000000000 ) ) ;
#4212=CARTESIAN_POINT ( 'NONE',  ( 0.000000000000000000, 2.755905511811024056, 0.000000000000000000 ) ) ;
#4285=CARTESIAN_POINT ( 'NONE',  ( -0.2042174104418111591, 2.755905511811024056, -0.3133417129078099328 ) ) ;
#4401=DIRECTION ( 'NONE',  ( 0.000000000000000000, 0.000000000000000000, 1.000000000000000000 ) ) ;
#4424=DIRECTION ( 'NONE',  ( 0.9990914673551315461, 0.000000000000000000, -0.04261736568783054679 ) ) ;
#4445=CYLINDRICAL_SURFACE ( 'NONE', #11484, 0.3740157480314960647 ) ;
#4549=LINE ( 'NONE', #151, #6635 ) ;
#4555=EDGE_CURVE ( 'NONE', #13306, #41806, #11066, .T. ) ;
#4561=CARTESIAN_POINT ( 'NONE',  ( 0.000000000000000000, 0.000000000000000000, 0.000000000000000000 ) ) ;
#4631=AXIS2_PLACEMENT_3D ( 'NONE', #32636, #25376, #40624 ) ;
#4662=LINE ( 'NONE', #40805, #3571 ) ;
#4686=EDGE_LOOP ( 'NONE', ( #18293, #28561, #25726, #19918 ) ) ;
#4802=CARTESIAN_POINT ( 'NONE',  ( 1.352759075253495258, 2.755905511811024056, 0.2762566512555730269 ) ) ;
#4897=CIRCLE ( 'NONE', #11497, 1.181102362204723200 ) ;
#5255=CARTESIAN_POINT ( 'NONE',  ( 4.580371886574746102E-17, 7.874015748031496287, 0.3740157480314960647 ) ) ;
#5410=ORIENTED_EDGE ( 'NONE', *, *, #14891, .F. ) ;
#5412=ADVANCED_FACE ( 'NONE', ( #42030 ), #42274, .F. ) ;
#5429=DIRECTION ( 'NONE',  ( 0.000000000000000000, 1.000000000000000000, 0.000000000000000000 ) ) ;
#5490=( CONVERSION_BASED_UNIT ( 'INCH', #41369 ) LENGTH_UNIT ( ) NAMED_UNIT ( #28098 ) );
#5539=PLANE ( 'NONE',  #45853 ) ;
#5592=CARTESIAN_POINT ( 'NONE',  ( -0.2480359799030329715, -0.6299212598425202314, 0.2799391584775194342 ) ) ;
#5650=CIRCLE ( 'NONE', #25434, 1.181102362204723200 ) ;
#5686=DIRECTION ( 'NONE',  ( 0.8660254037844432595, 0.000000000000000000, 0.4999999999999920064 ) ) ;
#5716=ORIENTED_EDGE ( 'NONE', *, *, #19757, .F. ) ;
#5891=DIRECTION ( 'NONE',  ( 0.000000000000000000, -1.000000000000000000, 0.000000000000000000 ) ) ;
#6063=LINE ( 'NONE', #40932, #16802 ) ;
#6065=DIRECTION ( 'NONE',  ( 0.000000000000000000, 0.000000000000000000, -1.000000000000000000 ) ) ;
#6117=PRODUCT_DEFINITION_CONTEXT ( 'detailed design', #26605, 'design' ) ;
#6126=ORIENTED_EDGE ( 'NONE', *, *, #29788, .T. ) ;
#6148=PLANE ( 'NONE',  #43551 ) ;
#6167=VECTOR ( 'NONE', #20655, 39.37007874015748143 ) ;
#6230=ORIENTED_EDGE ( 'NONE', *, *, #43146, .T. ) ;
#6327=DIRECTION ( 'NONE',  ( 0.000000000000000000, -1.000000000000000000, 0.000000000000000000 ) ) ;
#6377=ORIENTED_EDGE ( 'NONE', *, *, #12871, .T. ) ;
#6379=ORIENTED_EDGE ( 'NONE', *, *, #13843, .F. ) ;
#6579=ORIENTED_EDGE ( 'NONE', *, *, #1593, .T. ) ;
#6604=CARTESIAN_POINT ( 'NONE',  ( 1.157218145390799036, 2.755905511811024056, 0.2363238328731523952 ) ) ;
#6635=VECTOR ( 'NONE', #47621, 39.37007874015748143 ) ;
#6765=ORIENTED_EDGE ( 'NONE', *, *, #11894, .T. ) ;
#6766=ORIENTED_EDGE ( 'NONE', *, *, #29788, .F. ) ;
#6820=EDGE_LOOP ( 'NONE', ( #44127, #604, #8431, #6766 ) ) ;
#6891=ADVANCED_FACE ( 'NONE', ( #25932 ), #49130, .T. ) ;
#6959=PRODUCT_DEFINITION_FORMATION_WITH_SPECIFIED_SOURCE ( 'ANY', '', #40108, .NOT_KNOWN. ) ;
#7225=EDGE_CURVE ( 'NONE', #37788, #45331, #985, .T. ) ;
#7227=CYLINDRICAL_SURFACE ( 'NONE', #35851, 1.181102362204723200 ) ;
#7465=LINE ( 'NONE', #3592, #25310 ) ;
#7554=EDGE_CURVE ( 'NONE', #25081, #41228, #20651, .T. ) ;
#7562=DIRECTION ( 'NONE',  ( -0.000000000000000000, -1.000000000000000000, -0.000000000000000000 ) ) ;
#7581=DIRECTION ( 'NONE',  ( 0.000000000000000000, 0.000000000000000000, -1.000000000000000000 ) ) ;
#7616=CARTESIAN_POINT ( 'NONE',  ( 0.000000000000000000, 7.874015748031496287, 0.000000000000000000 ) ) ;
#7748=CARTESIAN_POINT ( 'NONE',  ( 0.3734705886643994721, -0.6299212598425202314, -0.02018660888377523527 ) ) ;
#7901=LINE ( 'NONE', #4802, #44207 ) ;
#7957=ORIENTED_EDGE ( 'NONE', *, *, #8082, .T. ) ;
#8082=EDGE_CURVE ( 'NONE', #49027, #10066, #45787, .T. ) ;
#8122=ORIENTED_EDGE ( 'NONE', *, *, #19872, .F. ) ;
#8159=ORIENTED_EDGE ( 'NONE', *, *, #30582, .F. ) ;
#8320=FACE_OUTER_BOUND ( 'NONE', #13981, .T. ) ;
#8396=AXIS2_PLACEMENT_3D ( 'NONE', #37820, #37564, #2447 ) ;
#8428=DIRECTION ( 'NONE',  ( -0.07365742419378766559, -0.000000000000000000, 0.9972836025229415702 ) ) ;
#8431=ORIENTED_EDGE ( 'NONE', *, *, #43146, .F. ) ;
#8439=VECTOR ( 'NONE', #39560, 39.37007874015748854 ) ;
#8445=LINE ( 'NONE', #39936, #49778 ) ;
#8650=CARTESIAN_POINT ( 'NONE',  ( 0.000000000000000000, 7.874015748031496287, -0.3740157480314960647 ) ) ;
#8662=AXIS2_PLACEMENT_3D ( 'NONE', #7616, #3236, #30357 ) ;
#8769=EDGE_CURVE ( 'NONE', #14380, #20677, #4662, .T. ) ;
#8789=DIRECTION ( 'NONE',  ( 0.000000000000000000, -1.000000000000000000, 0.000000000000000000 ) ) ;
#8833=ORIENTED_EDGE ( 'NONE', *, *, #13469, .T. ) ;
#8838=EDGE_CURVE ( 'NONE', #286, #37788, #16280, .T. ) ;
#8848=ADVANCED_FACE ( 'NONE', ( #40032 ), #789, .F. ) ;
#8876=DIRECTION ( 'NONE',  ( -0.000000000000000000, -1.000000000000000000, -0.000000000000000000 ) ) ;
#8887=AXIS2_PLACEMENT_3D ( 'NONE', #24937, #24430, #12549 ) ;
#8957=PLANE ( 'NONE',  #48207 ) ;
#8970=EDGE_CURVE ( 'NONE', #50620, #46022, #49765, .T. ) ;
#9067=AXIS2_PLACEMENT_3D ( 'NONE', #41662, #10419, #30547 ) ;
#9166=ORIENTED_EDGE ( 'NONE', *, *, #8970, .T. ) ;
#9323=VECTOR ( 'NONE', #32041, 39.37007874015748143 ) ;
#9547=ORIENTED_EDGE ( 'NONE', *, *, #24686, .F. ) ;
#9606=LINE ( 'NONE', #21478, #32754 ) ;
#9771=ORIENTED_EDGE ( 'NONE', *, *, #21668, .T. ) ;
#9788=DIRECTION ( 'NONE',  ( 0.000000000000000000, 0.000000000000000000, -1.000000000000000000 ) ) ;
#9873=ORIENTED_EDGE ( 'NONE', *, *, #21265, .F. ) ;
#9957=PLANE ( 'NONE',  #10553 ) ;
#10066=VERTEX_POINT ( 'NONE', #20371 ) ;
#10105=EDGE_CURVE ( 'NONE', #13306, #39823, #12628, .T. ) ;
#10198=UNCERTAINTY_MEASURE_WITH_UNIT (LENGTH_MEASURE( 1.000000000000000082E-05 ), #43383, 'distance_accuracy_value', 'NONE');
#10222=CARTESIAN_POINT ( 'NONE',  ( -0.06966273521059174190, 0.000000000000000000, 0.3674709282358790130 ) ) ;
#10378=DIRECTION ( 'NONE',  ( 0.000000000000000000, -1.000000000000000000, 0.000000000000000000 ) ) ;
#10419=DIRECTION ( 'NONE',  ( 0.000000000000000000, -1.000000000000000000, 0.000000000000000000 ) ) ;
#10481=DIRECTION ( 'NONE',  ( 0.000000000000000000, 0.000000000000000000, -1.000000000000000000 ) ) ;
#10492=EDGE_CURVE ( 'NONE', #2736, #23094, #23934, .T. ) ;
#10553=AXIS2_PLACEMENT_3D ( 'NONE', #25956, #41449, #45544 ) ;
#10585=ORIENTED_EDGE ( 'NONE', *, *, #39902, .F. ) ;
#10713=ADVANCED_FACE ( 'NONE', ( #13851 ), #45317, .T. ) ;
#10730=CARTESIAN_POINT ( 'NONE',  ( 0.000000000000000000, 2.755905511811024056, 0.000000000000000000 ) ) ;
#10819=ORIENTED_EDGE ( 'NONE', *, *, #17277, .T. ) ;
#11066=LINE ( 'NONE', #26800, #29659 ) ;
#11375=VECTOR ( 'NONE', #38254, 39.37007874015748854 ) ;
#11467=EDGE_LOOP ( 'NONE', ( #8833, #14753 ) ) ;
#11484=AXIS2_PLACEMENT_3D ( 'NONE', #31826, #7562, #35184 ) ;
#11497=AXIS2_PLACEMENT_3D ( 'NONE', #26468, #38359, #10481 ) ;
#11586=VERTEX_POINT ( 'NONE', #37735 ) ;
#11588=DIRECTION ( 'NONE',  ( 0.000000000000000000, 0.000000000000000000, -1.000000000000000000 ) ) ;
#11691=ADVANCED_FACE ( 'NONE', ( #38982 ), #40007, .F. ) ;
#11774=DIRECTION ( 'NONE',  ( 0.000000000000000000, -0.000000000000000000, 1.000000000000000000 ) ) ;
#11866=CARTESIAN_POINT ( 'NONE',  ( -0.1692531782225912829, -0.6299212598425202314, 0.3335283217915853138 ) ) ;
#11894=EDGE_CURVE ( 'NONE', #50620, #33133, #22615, .T. ) ;
#11931=DIRECTION ( 'NONE',  ( -0.04261736568783054679, -0.000000000000000000, -0.9990914673551315461 ) ) ;
#11934=DIMENSIONAL_EXPONENTS ( 1.000000000000000000, 0.000000000000000000, 0.000000000000000000, 0.000000000000000000, 0.000000000000000000, 0.000000000000000000, 0.000000000000000000 ) ;
#12026=ORIENTED_EDGE ( 'NONE', *, *, #42959, .F. ) ;
#12094=CARTESIAN_POINT ( 'NONE',  ( 0.000000000000000000, 0.000000000000000000, 0.000000000000000000 ) ) ;
#12159=CIRCLE ( 'NONE', #8887, 0.3740157480314960647 ) ;
#12183=ORIENTED_EDGE ( 'NONE', *, *, #43624, .F. ) ;
#12206=CARTESIAN_POINT ( 'NONE',  ( -1.022351642223462997E-16, 0.000000000000000000, -9.058396573151636093E-17 ) ) ;
#12243=PLANE ( 'NONE',  #32528 ) ;
#12273=LINE ( 'NONE', #8650, #40279 ) ;
#12290=ADVANCED_FACE ( 'NONE', ( #45261 ), #5539, .T. ) ;
#12402=AXIS2_PLACEMENT_3D ( 'NONE', #32183, #15901, #11774 ) ;
#12549=DIRECTION ( 'NONE',  ( 0.000000000000000000, 0.000000000000000000, -1.000000000000000000 ) ) ;
#12628=LINE ( 'NONE', #32524, #16883 ) ;
#12635=ORIENTED_EDGE ( 'NONE', *, *, #24287, .T. ) ;
#12682=FACE_OUTER_BOUND ( 'NONE', #26018, .T. ) ;
#12683=CARTESIAN_POINT ( 'NONE',  ( -1.004926760980926259, 2.755905511811024056, -0.6205843980233154422 ) ) ;
#12715=VECTOR ( 'NONE', #36180, 39.37007874015748854 ) ;
#12799=DIRECTION ( 'NONE',  ( 0.9797780297642104674, 0.000000000000000000, 0.2000875118326023161 ) ) ;
#12871=EDGE_CURVE ( 'NONE', #16212, #39823, #431, .T. ) ;
#12895=VECTOR ( 'NONE', #50286, 39.37007874015748143 ) ;
#12906=EDGE_CURVE ( 'NONE', #36716, #45331, #39242, .T. ) ;
#12912=PRODUCT_DEFINITION_SHAPE ( 'NONE', 'NONE',  #24694 ) ;
#12925=CARTESIAN_POINT ( 'NONE',  ( -0.03497847339001228933, 2.755905511811024056, 1.180584302963952448 ) ) ;
#12983=LINE ( 'NONE', #16603, #34025 ) ;
#12997=CARTESIAN_POINT ( 'NONE',  ( 0.3530705266098149719, 0.000000000000000000, -0.1234057657284600290 ) ) ;
#13126=MECHANICAL_DESIGN_GEOMETRIC_PRESENTATION_REPRESENTATION('',(#46045),#42776);
#13189=ORIENTED_EDGE ( 'NONE', *, *, #26379, .T. ) ;
#13235=DIRECTION ( 'NONE',  ( 0.8660254037844431485, 0.000000000000000000, 0.4999999999999918954 ) ) ;
#13306=VERTEX_POINT ( 'NONE', #10222 ) ;
#13371=FACE_OUTER_BOUND ( 'NONE', #16908, .T. ) ;
#13469=EDGE_CURVE ( 'NONE', #33133, #25081, #26050, .T. ) ;
#13483=CARTESIAN_POINT ( 'NONE',  ( 0.000000000000000000, 2.755905511811022723, 0.000000000000000000 ) ) ;
#13615=CIRCLE ( 'NONE', #16894, 0.3740157480314960647 ) ;
#13635=ORIENTED_EDGE ( 'NONE', *, *, #26379, .F. ) ;
#13691=ORIENTED_EDGE ( 'NONE', *, *, #2021, .F. ) ;
#13708=CARTESIAN_POINT ( 'NONE',  ( 0.04573806838996180568, 0.000000000000000000, 0.07195353765596652906 ) ) ;
#13843=EDGE_CURVE ( 'NONE', #43306, #1528, #45813, .T. ) ;
#13851=FACE_OUTER_BOUND ( 'NONE', #976, .T. ) ;
#13881=PLANE ( 'NONE',  #31020 ) ;
#13898=CARTESIAN_POINT ( 'NONE',  ( 0.000000000000000000, 2.755905511811024056, 0.000000000000000000 ) ) ;
#13980=ADVANCED_FACE ( 'NONE', ( #13371 ), #13881, .T. ) ;
#13981=EDGE_LOOP ( 'NONE', ( #12183, #8122, #22378, #26957, #26295, #10585, #18726, #19043, #14023, #49965 ) ) ;
#14023=ORIENTED_EDGE ( 'NONE', *, *, #47947, .F. ) ;
#14071=FACE_OUTER_BOUND ( 'NONE', #42593, .T. ) ;
#14187=CARTESIAN_POINT ( 'NONE',  ( 0.000000000000000000, 2.755905511811024056, 0.000000000000000000 ) ) ;
#14249=EDGE_CURVE ( 'NONE', #20677, #48779, #7901, .T. ) ;
#14251=DIRECTION ( 'NONE',  ( 0.000000000000000000, -1.000000000000000000, 0.000000000000000000 ) ) ;
#14312=EDGE_CURVE ( 'NONE', #45331, #33133, #23906, .T. ) ;
#14375=ORIENTED_EDGE ( 'NONE', *, *, #13843, .T. ) ;
#14380=VERTEX_POINT ( 'NONE', #24931 ) ;
#14419=CARTESIAN_POINT ( 'NONE',  ( 0.000000000000000000, 2.755905511811024056, 0.000000000000000000 ) ) ;
#14449=VECTOR ( 'NONE', #47944, 39.37007874015748854 ) ;
#14454=CARTESIAN_POINT ( 'NONE',  ( -0.1613169216229337344, 0.000000000000000000, -0.3340583758975808060 ) ) ;
#14526=CARTESIAN_POINT ( 'NONE',  ( 0.3530705266098149164, -0.6299212598425202314, -0.1234057657284599735 ) ) ;
#14618=EDGE_LOOP ( 'NONE', ( #25964, #16737, #39308, #46887 ) ) ;
#14667=FACE_OUTER_BOUND ( 'NONE', #46738, .T. ) ;
#14751=DIRECTION ( 'NONE',  ( 0.000000000000000000, 0.000000000000000000, 1.000000000000000000 ) ) ;
#14753=ORIENTED_EDGE ( 'NONE', *, *, #833, .F. ) ;
#14779=PLANE ( 'NONE',  #45008 ) ;
#14891=EDGE_CURVE ( 'NONE', #36899, #22341, #31023, .T. ) ;
#14982=ORIENTED_EDGE ( 'NONE', *, *, #30582, .T. ) ;
#15005=CARTESIAN_POINT ( 'NONE',  ( -0.1184164328040565317, 2.755905511811024056, -0.3547750388873516791 ) ) ;
#15226=CARTESIAN_POINT ( 'NONE',  ( -0.03497847339001228933, 2.755905511811024056, 1.180584302963952226 ) ) ;
#15250=CARTESIAN_POINT ( 'NONE',  ( -0.9156248155784967313, -0.6299212598425202314, 1.033395398741681293 ) ) ;
#15404=AXIS2_PLACEMENT_3D ( 'NONE', #27632, #46721, #15763 ) ;
#15406=CARTESIAN_POINT ( 'NONE',  ( -0.2480359799030329715, 2.755905511811024056, 0.2799391584775194342 ) ) ;
#15523=( NAMED_UNIT ( * ) SI_UNIT ( $, .STERADIAN. ) SOLID_ANGLE_UNIT ( ) );
#15763=DIRECTION ( 'NONE',  ( 0.000000000000000000, 0.000000000000000000, -1.000000000000000000 ) ) ;
#15774=CARTESIAN_POINT ( 'NONE',  ( -0.3739466299075467348, 2.755905511811024056, -1.120342228065320134 ) ) ;
#15857=DIRECTION ( 'NONE',  ( 0.000000000000000000, -1.000000000000000000, 0.000000000000000000 ) ) ;
#15901=DIRECTION ( 'NONE',  ( 0.000000000000000000, 1.000000000000000000, 0.000000000000000000 ) ) ;
#15935=ORIENTED_EDGE ( 'NONE', *, *, #47947, .T. ) ;
#16018=SHAPE_DEFINITION_REPRESENTATION ( #12912, #34429 ) ;
#16029=LENGTH_MEASURE_WITH_UNIT ( LENGTH_MEASURE( 0.02539999999999999897 ), #23262 );
#16104=PLANE ( 'NONE',  #50042 ) ;
#16114=LINE ( 'NONE', #5255, #31258 ) ;
#16135=ORIENTED_EDGE ( 'NONE', *, *, #34832, .F. ) ;
#16198=ORIENTED_EDGE ( 'NONE', *, *, #44567, .F. ) ;
#16212=VERTEX_POINT ( 'NONE', #38288 ) ;
#16235=ADVANCED_FACE ( 'NONE', ( #12682 ), #48002, .F. ) ;
#16239=EDGE_CURVE ( 'NONE', #41806, #286, #50835, .T. ) ;
#16280=LINE ( 'NONE', #28400, #9323 ) ;
#16372=VECTOR ( 'NONE', #34538, 39.37007874015747433 ) ;
#16579=LINE ( 'NONE', #19410, #49421 ) ;
#16603=CARTESIAN_POINT ( 'NONE',  ( 1.039905234370930742, 2.755905511811024056, -0.5599999049406324536 ) ) ;
#16635=ORIENTED_EDGE ( 'NONE', *, *, #12906, .F. ) ;
#16712=CARTESIAN_POINT ( 'NONE',  ( 0.3734705886643994721, -0.6299212598425202314, -0.02018660888377523527 ) ) ;
#16714=ORIENTED_EDGE ( 'NONE', *, *, #30239, .T. ) ;
#16737=ORIENTED_EDGE ( 'NONE', *, *, #8838, .T. ) ;
#16767=ORIENTED_EDGE ( 'NONE', *, *, #7225, .T. ) ;
#16793=EDGE_LOOP ( 'NONE', ( #47794, #32393, #48114, #40746 ) ) ;
#16802=VECTOR ( 'NONE', #22071, 39.37007874015748854 ) ;
#16810=VECTOR ( 'NONE', #31533, 39.37007874015748143 ) ;
#16873=ORIENTED_EDGE ( 'NONE', *, *, #25807, .F. ) ;
#16883=VECTOR ( 'NONE', #20628, 39.37007874015748143 ) ;
#16885=AXIS2_PLACEMENT_3D ( 'NONE', #13898, #5891, #42026 ) ;
#16894=AXIS2_PLACEMENT_3D ( 'NONE', #43880, #36163, #4401 ) ;
#16908=EDGE_LOOP ( 'NONE', ( #40637, #35884 ) ) ;
#16914=ORIENTED_EDGE ( 'NONE', *, *, #17339, .T. ) ;
#16964=ORIENTED_EDGE ( 'NONE', *, *, #29827, .T. ) ;
#17011=CARTESIAN_POINT ( 'NONE',  ( -1.004926760980926481, 0.000000000000000000, -0.6205843980233154422 ) ) ;
#17076=CIRCLE ( 'NONE', #2958, 0.3740157480314960647 ) ;
#17117=ADVANCED_FACE ( 'NONE', ( #31876 ), #12243, .T. ) ;
#17277=EDGE_CURVE ( 'NONE', #1528, #24292, #40545, .T. ) ;
#17339=EDGE_CURVE ( 'NONE', #40993, #26527, #13615, .T. ) ;
#17399=DIRECTION ( 'NONE',  ( 0.000000000000000000, 0.000000000000000000, -1.000000000000000000 ) ) ;
#17476=CARTESIAN_POINT ( 'NONE',  ( 0.3664524127070866721, -0.6299212598425202314, 0.07483588040983164824 ) ) ;
#17479=VECTOR ( 'NONE', #22346, 39.37007874015748143 ) ;
#17530=CARTESIAN_POINT ( 'NONE',  ( 0.000000000000000000, 2.755905511811024056, 0.000000000000000000 ) ) ;
#17547=VECTOR ( 'NONE', #19137, 39.37007874015748143 ) ;
#17551=EDGE_CURVE ( 'NONE', #46022, #25081, #23413, .T. ) ;
#17648=ADVANCED_FACE ( 'NONE', ( #20577 ), #8957, .F. ) ;
#17877=CIRCLE ( 'NONE', #547, 0.3740157480314960647 ) ;
#17909=ORIENTED_EDGE ( 'NONE', *, *, #33596, .T. ) ;
#17979=ORIENTED_EDGE ( 'NONE', *, *, #8082, .F. ) ;
#17990=CIRCLE ( 'NONE', #1477, 0.3740157480314960647 ) ;
#18077=CARTESIAN_POINT ( 'NONE',  ( 0.000000000000000000, 7.874015748031496287, 0.000000000000000000 ) ) ;
#18293=ORIENTED_EDGE ( 'NONE', *, *, #10105, .T. ) ;
#18316=LINE ( 'NONE', #2826, #50901 ) ;
#18393=VECTOR ( 'NONE', #30198, 39.37007874015748854 ) ;
#18726=ORIENTED_EDGE ( 'NONE', *, *, #7225, .F. ) ;
#18743=DIRECTION ( 'NONE',  ( 0.000000000000000000, -1.000000000000000000, 0.000000000000000000 ) ) ;
#18783=CARTESIAN_POINT ( 'NONE',  ( 1.295655976102049600E-16, 0.000000000000000000, -4.324626651086886948E-17 ) ) ;
#18791=DIRECTION ( 'NONE',  ( 0.9797780297642105785, 0.000000000000000000, 0.2000875118326022883 ) ) ;
#18838=DIRECTION ( 'NONE',  ( 0.8865472742777344983, -0.000000000000000000, 0.4626380123495248964 ) ) ;
#18858=ADVANCED_FACE ( 'NONE', ( #24719 ), #25471, .F. ) ;
#18877=DIRECTION ( 'NONE',  ( -0.7484689079293680436, 0.000000000000000000, -0.6631698831091618063 ) ) ;
#19043=ORIENTED_EDGE ( 'NONE', *, *, #2595, .F. ) ;
#19137=DIRECTION ( 'NONE',  ( 0.000000000000000000, -1.000000000000000000, 0.000000000000000000 ) ) ;
#19271=LINE ( 'NONE', #39408, #40867 ) ;
#19344=ORIENTED_EDGE ( 'NONE', *, *, #21668, .F. ) ;
#19410=CARTESIAN_POINT ( 'NONE',  ( -0.06966273521059175577, 2.755905511811024056, 0.3674709282358789575 ) ) ;
#19652=CLOSED_SHELL ( 'NONE', ( #10713, #3166, #31550, #44419, #13980, #49978, #501, #42388, #36409, #42149, #42895, #23224, #12290, #17117, #18858, #46186, #5412, #25873, #3710, #21950, #6891, #8848, #37924, #28188, #21650, #17648, #11691, #19969, #16235 ) ) ;
#19708=ORIENTED_EDGE ( 'NONE', *, *, #17551, .T. ) ;
#19757=EDGE_CURVE ( 'NONE', #32113, #2736, #9606, .T. ) ;
#19853=DIRECTION ( 'NONE',  ( 0.3226000110797114795, 0.000000000000000000, -0.9465353838348411486 ) ) ;
#19872=EDGE_CURVE ( 'NONE', #26527, #40993, #17076, .T. ) ;
#19903=CARTESIAN_POINT ( 'NONE',  ( 0.3734705886643994721, 2.755905511811024056, -0.02018660888377523527 ) ) ;
#19918=ORIENTED_EDGE ( 'NONE', *, *, #4555, .F. ) ;
#19947=LINE ( 'NONE', #3968, #29450 ) ;
#19969=ADVANCED_FACE ( 'NONE', ( #35128 ), #50306, .F. ) ;
#20016=DIRECTION ( 'NONE',  ( 0.7526474967735860000, -0.000000000000000000, -0.6584236824419781309 ) ) ;
#20035=CARTESIAN_POINT ( 'NONE',  ( -0.1692531782225912829, 2.755905511811024056, 0.3335283217915853138 ) ) ;
#20047=ORIENTED_EDGE ( 'NONE', *, *, #19757, .T. ) ;
#20180=EDGE_LOOP ( 'NONE', ( #6765, #35168, #44548, #34432 ) ) ;
#20194=PLANE ( 'NONE',  #22987 ) ;
#20222=FACE_OUTER_BOUND ( 'NONE', #37211, .T. ) ;
#20285=CIRCLE ( 'NONE', #4631, 1.181102362204723200 ) ;
#20371=CARTESIAN_POINT ( 'NONE',  ( -0.7832715154832613491, 0.000000000000000000, 0.8840183951921659622 ) ) ;
#20421=CARTESIAN_POINT ( 'NONE',  ( -0.1692531782225912829, -0.6299212598425202314, 0.3335283217915853138 ) ) ;
#20462=EDGE_LOOP ( 'NONE', ( #13189, #27916 ) ) ;
#20467=DIRECTION ( 'NONE',  ( 0.000000000000000000, 0.000000000000000000, 1.000000000000000000 ) ) ;
#20500=DIRECTION ( 'NONE',  ( -0.000000000000000000, -1.000000000000000000, 0.000000000000000000 ) ) ;
#20577=FACE_OUTER_BOUND ( 'NONE', #14618, .T. ) ;
#20628=DIRECTION ( 'NONE',  ( -0.000000000000000000, 1.000000000000000000, -0.000000000000000000 ) ) ;
#20651=LINE ( 'NONE', #1035, #198 ) ;
#20655=DIRECTION ( 'NONE',  ( -0.000000000000000000, 1.000000000000000000, -0.000000000000000000 ) ) ;
#20677=VERTEX_POINT ( 'NONE', #20884 ) ;
#20789=ORIENTED_EDGE ( 'NONE', *, *, #27278, .T. ) ;
#20843=EDGE_LOOP ( 'NONE', ( #16135, #43939, #16767, #37053 ) ) ;
#20846=ORIENTED_EDGE ( 'NONE', *, *, #33596, .F. ) ;
#20884=CARTESIAN_POINT ( 'NONE',  ( 0.3664524127070866721, 2.755905511811024056, 0.07483588040983164824 ) ) ;
#20984=CARTESIAN_POINT ( 'NONE',  ( 0.000000000000000000, 0.000000000000000000, 0.000000000000000000 ) ) ;
#21054=CARTESIAN_POINT ( 'NONE',  ( -0.2042174104418111591, 0.000000000000000000, -0.3133417129078099328 ) ) ;
#21064=EDGE_CURVE ( 'NONE', #25081, #41000, #17877, .T. ) ;
#21100=DIRECTION ( 'NONE',  ( -0.9972836025229415702, 0.000000000000000000, -0.07365742419378766559 ) ) ;
#21265=EDGE_CURVE ( 'NONE', #32836, #24066, #19947, .T. ) ;
#21274=CARTESIAN_POINT ( 'NONE',  ( 0.000000000000000000, 2.755905511811022723, 0.000000000000000000 ) ) ;
#21327=ORIENTED_EDGE ( 'NONE', *, *, #14249, .F. ) ;
#21478=CARTESIAN_POINT ( 'NONE',  ( 0.3632705576371071388, 0.000000000000000000, -0.07179618730611768418 ) ) ;
#21650=ADVANCED_FACE ( 'NONE', ( #42626 ), #30260, .T. ) ;
#21668=EDGE_CURVE ( 'NONE', #10066, #32836, #37686, .T. ) ;
#21708=VECTOR ( 'NONE', #47276, 39.37007874015748854 ) ;
#21740=DIRECTION ( 'NONE',  ( 0.000000000000000000, -1.000000000000000000, 0.000000000000000000 ) ) ;
#21783=FACE_OUTER_BOUND ( 'NONE', #23705, .T. ) ;
#21881=DIRECTION ( 'NONE',  ( 0.000000000000000000, -1.000000000000000000, 0.000000000000000000 ) ) ;
#21901=CARTESIAN_POINT ( 'NONE',  ( 0.000000000000000000, 2.755905511811024056, 0.000000000000000000 ) ) ;
#21902=AXIS2_PLACEMENT_3D ( 'NONE', #15250, #18877, #35383 ) ;
#21950=ADVANCED_FACE ( 'NONE', ( #50700 ), #27261, .T. ) ;
#21971=VECTOR ( 'NONE', #20016, 39.37007874015748143 ) ;
#22071=DIRECTION ( 'NONE',  ( -0.04261736568783053986, 0.000000000000000000, -0.9990914673551313241 ) ) ;
#22164=DIRECTION ( 'NONE',  ( -0.2000875118326022883, -0.000000000000000000, 0.9797780297642105785 ) ) ;
#22298=CYLINDRICAL_SURFACE ( 'NONE', #9067, 1.181102362204723200 ) ;
#22341=VERTEX_POINT ( 'NONE', #49901 ) ;
#22346=DIRECTION ( 'NONE',  ( 0.000000000000000000, -1.000000000000000000, -0.000000000000000000 ) ) ;
#22378=ORIENTED_EDGE ( 'NONE', *, *, #113, .T. ) ;
#22469=LINE ( 'NONE', #41839, #12895 ) ;
#22502=CARTESIAN_POINT ( 'NONE',  ( 0.000000000000000000, 2.755905511811024056, 0.000000000000000000 ) ) ;
#22583=VECTOR ( 'NONE', #12799, 39.37007874015748143 ) ;
#22615=LINE ( 'NONE', #27235, #38405 ) ;
#22736=ORIENTED_EDGE ( 'NONE', *, *, #40002, .T. ) ;
#22965=CARTESIAN_POINT ( 'NONE',  ( 0.000000000000000000, 2.755905511811024056, 0.000000000000000000 ) ) ;
#22987=AXIS2_PLACEMENT_3D ( 'NONE', #28194, #24847, #40082 ) ;
#23094=VERTEX_POINT ( 'NONE', #44661 ) ;
#23121=ORIENTED_EDGE ( 'NONE', *, *, #17277, .F. ) ;
#23224=ADVANCED_FACE ( 'NONE', ( #30966 ), #7227, .T. ) ;
#23262=( LENGTH_UNIT ( ) NAMED_UNIT ( * ) SI_UNIT ( $, .METRE. ) );
#23406=DIRECTION ( 'NONE',  ( -0.8660254037844362651, 0.000000000000000000, 0.5000000000000039968 ) ) ;
#23413=LINE ( 'NONE', #50478, #30086 ) ;
#23648=EDGE_CURVE ( 'NONE', #23094, #20677, #19271, .T. ) ;
#23705=EDGE_LOOP ( 'NONE', ( #15935, #32533 ) ) ;
#23754=ORIENTED_EDGE ( 'NONE', *, *, #21265, .T. ) ;
#23802=ORIENTED_EDGE ( 'NONE', *, *, #113, .F. ) ;
#23906=LINE ( 'NONE', #4285, #21971 ) ;
#23934=LINE ( 'NONE', #16712, #28396 ) ;
#23948=AXIS2_PLACEMENT_3D ( 'NONE', #38172, #22164, #18791 ) ;
#23992=VERTEX_POINT ( 'NONE', #3918 ) ;
#24042=DIRECTION ( 'NONE',  ( -0.04261736568783053986, 0.000000000000000000, -0.9990914673551313241 ) ) ;
#24066=VERTEX_POINT ( 'NONE', #12683 ) ;
#24091=DIRECTION ( 'NONE',  ( 0.000000000000000000, 1.000000000000000000, -0.000000000000000000 ) ) ;
#24093=ORIENTED_EDGE ( 'NONE', *, *, #48615, .F. ) ;
#24287=EDGE_CURVE ( 'NONE', #41806, #24641, #22469, .T. ) ;
#24292=VERTEX_POINT ( 'NONE', #15226 ) ;
#24403=DIRECTION ( 'NONE',  ( -0.000000000000000000, -1.000000000000000000, -0.000000000000000000 ) ) ;
#24430=DIRECTION ( 'NONE',  ( 0.000000000000000000, -1.000000000000000000, 0.000000000000000000 ) ) ;
#24538=DIRECTION ( 'NONE',  ( 0.000000000000000000, -0.000000000000000000, -1.000000000000000000 ) ) ;
#24594=LINE ( 'NONE', #12206, #21708 ) ;
#24641=VERTEX_POINT ( 'NONE', #38888 ) ;
#24659=AXIS2_PLACEMENT_3D ( 'NONE', #45536, #25431, #30074 ) ;
#24678=UNCERTAINTY_MEASURE_WITH_UNIT (LENGTH_MEASURE( 1.000000000000000082E-05 ), #5490, 'distance_accuracy_value', 'NONE');
#24681=DIRECTION ( 'NONE',  ( 0.9797780297642104674, 0.000000000000000000, 0.2000875118326022606 ) ) ;
#24686=EDGE_CURVE ( 'NONE', #41228, #36899, #33513, .T. ) ;
#24694=PRODUCT_DEFINITION ( 'UNKNOWN', '', #6959, #6117 ) ;
#24719=FACE_OUTER_BOUND ( 'NONE', #47906, .T. ) ;
#24749=EDGE_CURVE ( 'NONE', #24066, #45331, #7465, .T. ) ;
#24847=DIRECTION ( 'NONE',  ( 0.4348526007323283427, 0.000000000000000000, 0.9005016466594218949 ) ) ;
#24931=CARTESIAN_POINT ( 'NONE',  ( 0.3664524127070866721, 0.000000000000000000, 0.07483588040983164824 ) ) ;
#24937=CARTESIAN_POINT ( 'NONE',  ( 0.000000000000000000, 2.755905511811024056, 0.000000000000000000 ) ) ;
#24952=AXIS2_PLACEMENT_3D ( 'NONE', #14419, #2797, #9788 ) ;
#25081=VERTEX_POINT ( 'NONE', #50208 ) ;
#25193=ORIENTED_EDGE ( 'NONE', *, *, #34832, .T. ) ;
#25281=ORIENTED_EDGE ( 'NONE', *, *, #49878, .F. ) ;
#25310=VECTOR ( 'NONE', #18838, 39.37007874015748854 ) ;
#25350=DIRECTION ( 'NONE',  ( 0.1938878870612535943, 0.000000000000000000, 0.9810236935216818388 ) ) ;
#25376=DIRECTION ( 'NONE',  ( 0.000000000000000000, -1.000000000000000000, 0.000000000000000000 ) ) ;
#25431=DIRECTION ( 'NONE',  ( 0.9485564197619719140, 0.000000000000000000, -0.3166081466550567658 ) ) ;
#25434=AXIS2_PLACEMENT_3D ( 'NONE', #4561, #36574, #47884 ) ;
#25471=PLANE ( 'NONE',  #48275 ) ;
#25490=EDGE_LOOP ( 'NONE', ( #25193, #9873, #19344, #17979 ) ) ;
#25586=ORIENTED_EDGE ( 'NONE', *, *, #25807, .T. ) ;
#25608=DIRECTION ( 'NONE',  ( 0.000000000000000000, 0.000000000000000000, -1.000000000000000000 ) ) ;
#25726=ORIENTED_EDGE ( 'NONE', *, *, #16239, .F. ) ;
#25807=EDGE_CURVE ( 'NONE', #36899, #11586, #20285, .T. ) ;
#25873=ADVANCED_FACE ( 'NONE', ( #33900 ), #14779, .F. ) ;
#25932=FACE_OUTER_BOUND ( 'NONE', #25490, .T. ) ;
#25956=CARTESIAN_POINT ( 'NONE',  ( -0.2834077913992259501, -0.6299212598425202314, -0.2440651625074179987 ) ) ;
#25964=ORIENTED_EDGE ( 'NONE', *, *, #16239, .T. ) ;
#26018=EDGE_LOOP ( 'NONE', ( #10819, #1378, #42669, #29189 ) ) ;
#26050=CIRCLE ( 'NONE', #1282, 0.3740157480314960647 ) ;
#26118=CIRCLE ( 'NONE', #32741, 0.3740157480314961203 ) ;
#26126=( LENGTH_UNIT ( ) NAMED_UNIT ( * ) SI_UNIT ( $, .METRE. ) );
#26295=ORIENTED_EDGE ( 'NONE', *, *, #13469, .F. ) ;
#26379=EDGE_CURVE ( 'NONE', #23094, #20677, #26118, .T. ) ;
#26466=DIRECTION ( 'NONE',  ( -0.000000000000000000, -1.000000000000000000, 0.000000000000000000 ) ) ;
#26468=CARTESIAN_POINT ( 'NONE',  ( 0.000000000000000000, 2.755905511811024056, 0.000000000000000000 ) ) ;
#26521=DIRECTION ( 'NONE',  ( 0.000000000000000000, -0.000000000000000000, -1.000000000000000000 ) ) ;
#26527=VERTEX_POINT ( 'NONE', #45055 ) ;
#26605=APPLICATION_CONTEXT ( 'automotive_design' ) ;
#26719=DIRECTION ( 'NONE',  ( 0.8660254037844432595, 0.000000000000000000, 0.4999999999999920064 ) ) ;
#26741=AXIS2_PLACEMENT_3D ( 'NONE', #20984, #20467, #36229 ) ;
#26762=CARTESIAN_POINT ( 'NONE',  ( -0.1692531782225912829, 0.000000000000000000, 0.3335283217915853138 ) ) ;
#26800=CARTESIAN_POINT ( 'NONE',  ( -0.1194579567165914291, 0.000000000000000000, 0.3504996250137321634 ) ) ;
#26957=ORIENTED_EDGE ( 'NONE', *, *, #21064, .F. ) ;
#26960=ORIENTED_EDGE ( 'NONE', *, *, #30405, .F. ) ;
#26978=CARTESIAN_POINT ( 'NONE',  ( 0.000000000000000000, 2.755905511811024056, 0.000000000000000000 ) ) ;
#27226=DIRECTION ( 'NONE',  ( 0.000000000000000000, 0.000000000000000000, -1.000000000000000000 ) ) ;
#27235=CARTESIAN_POINT ( 'NONE',  ( -0.2042174104418111591, -0.6299212598425202314, -0.3133417129078099328 ) ) ;
#27261=PLANE ( 'NONE',  #29179 ) ;
#27278=EDGE_CURVE ( 'NONE', #46126, #23094, #35421, .T. ) ;
#27300=EDGE_LOOP ( 'NONE', ( #37302, #39045 ) ) ;
#27366=LINE ( 'NONE', #15005, #11375 ) ;
#27519=ORIENTED_EDGE ( 'NONE', *, *, #30405, .T. ) ;
#27528=DIRECTION ( 'NONE',  ( 0.000000000000000000, -1.000000000000000000, -0.000000000000000000 ) ) ;
#27600=ORIENTED_EDGE ( 'NONE', *, *, #50660, .T. ) ;
#27632=CARTESIAN_POINT ( 'NONE',  ( 0.000000000000000000, 0.000000000000000000, 0.000000000000000000 ) ) ;
#27673=CARTESIAN_POINT ( 'NONE',  ( 0.03944455730724595599, 0.000000000000000000, -0.07558709797372036021 ) ) ;
#27831=CIRCLE ( 'NONE', #3112, 1.181102362204723200 ) ;
#27916=ORIENTED_EDGE ( 'NONE', *, *, #23648, .F. ) ;
#27982=CARTESIAN_POINT ( 'NONE',  ( 0.000000000000000000, 2.755905511811022723, 0.000000000000000000 ) ) ;
#28098=DIMENSIONAL_EXPONENTS ( 1.000000000000000000, 0.000000000000000000, 0.000000000000000000, 0.000000000000000000, 0.000000000000000000, 0.000000000000000000, 0.000000000000000000 ) ;
#28188=ADVANCED_FACE ( 'NONE', ( #21783 ), #45002, .T. ) ;
#28194=CARTESIAN_POINT ( 'NONE',  ( -0.1184164328040565317, -0.6299212598425202314, -0.3547750388873516791 ) ) ;
#28339=ORIENTED_EDGE ( 'NONE', *, *, #10492, .F. ) ;
#28355=DIRECTION ( 'NONE',  ( 0.000000000000000000, 1.000000000000000000, 0.000000000000000000 ) ) ;
#28396=VECTOR ( 'NONE', #44560, 39.37007874015748143 ) ;
#28399=VECTOR ( 'NONE', #28355, 39.37007874015748143 ) ;
#28400=CARTESIAN_POINT ( 'NONE',  ( -0.2480359799030329715, 2.755905511811024056, 0.2799391584775194342 ) ) ;
#28412=LINE ( 'NONE', #13708, #12715 ) ;
#28455=DIRECTION ( 'NONE',  ( -0.000000000000000000, 1.000000000000000000, 0.000000000000000000 ) ) ;
#28561=ORIENTED_EDGE ( 'NONE', *, *, #30695, .T. ) ;
#28747=ORIENTED_EDGE ( 'NONE', *, *, #1593, .F. ) ;
#28792=LINE ( 'NONE', #39644, #22583 ) ;
#28871=CARTESIAN_POINT ( 'NONE',  ( 0.3530705266098149164, -0.6299212598425202314, -0.1234057657284599735 ) ) ;
#29179=AXIS2_PLACEMENT_3D ( 'NONE', #18077, #31402, #37958 ) ;
#29189=ORIENTED_EDGE ( 'NONE', *, *, #50740, .F. ) ;
#29450=VECTOR ( 'NONE', #24091, 39.37007874015748143 ) ;
#29545=DIRECTION ( 'NONE',  ( -0.8660254037844362651, 0.000000000000000000, 0.5000000000000041078 ) ) ;
#29649=ORIENTED_EDGE ( 'NONE', *, *, #35228, .F. ) ;
#29659=VECTOR ( 'NONE', #42550, 39.37007874015748854 ) ;
#29788=EDGE_CURVE ( 'NONE', #41228, #23992, #28, .T. ) ;
#29827=EDGE_CURVE ( 'NONE', #945, #32113, #28412, .T. ) ;
#29930=AXIS2_PLACEMENT_3D ( 'NONE', #44146, #8789, #24538 ) ;
#30009=AXIS2_PLACEMENT_3D ( 'NONE', #44165, #4424, #24042 ) ;
#30068=CARTESIAN_POINT ( 'NONE',  ( -0.03497847339001226852, 0.000000000000000000, 1.180584302963952448 ) ) ;
#30074=DIRECTION ( 'NONE',  ( -0.3166081466550567658, 0.000000000000000000, -0.9485564197619719140 ) ) ;
#30086=VECTOR ( 'NONE', #30926, 39.37007874015748143 ) ;
#30198=DIRECTION ( 'NONE',  ( 0.9005016466594218949, 0.000000000000000000, -0.4348526007323282871 ) ) ;
#30204=CARTESIAN_POINT ( 'NONE',  ( -0.3739466299075467348, 2.755905511811024056, -1.120342228065320134 ) ) ;
#30239=EDGE_CURVE ( 'NONE', #32113, #46126, #47946, .T. ) ;
#30260=PLANE ( 'NONE',  #2224 ) ;
#30357=DIRECTION ( 'NONE',  ( 0.000000000000000000, 0.000000000000000000, -1.000000000000000000 ) ) ;
#30405=EDGE_CURVE ( 'NONE', #48779, #24292, #46510, .T. ) ;
#30496=CARTESIAN_POINT ( 'NONE',  ( 0.3530705266098149164, 2.755905511811024056, -0.1234057657284599735 ) ) ;
#30547=DIRECTION ( 'NONE',  ( 0.000000000000000000, 0.000000000000000000, -1.000000000000000000 ) ) ;
#30582=EDGE_CURVE ( 'NONE', #46126, #23094, #40767, .T. ) ;
#30695=EDGE_CURVE ( 'NONE', #39823, #286, #942, .T. ) ;
#30704=ORIENTED_EDGE ( 'NONE', *, *, #23648, .T. ) ;
#30792=DIRECTION ( 'NONE',  ( 0.7526474967735860000, 0.000000000000000000, -0.6584236824419781309 ) ) ;
#30872=DIRECTION ( 'NONE',  ( 0.000000000000000000, 0.000000000000000000, -1.000000000000000000 ) ) ;
#30926=DIRECTION ( 'NONE',  ( 0.000000000000000000, 1.000000000000000000, 0.000000000000000000 ) ) ;
#30966=FACE_OUTER_BOUND ( 'NONE', #44783, .T. ) ;
#30999=CARTESIAN_POINT ( 'NONE',  ( -0.1184164328040565317, 0.000000000000000000, -0.3547750388873516791 ) ) ;
#31011=ADVANCED_BREP_SHAPE_REPRESENTATION ( '', ( #41044, #26741 ), #43195 ) ;
#31020=AXIS2_PLACEMENT_3D ( 'NONE', #45347, #21881, #48942 ) ;
#31023=LINE ( 'NONE', #3147, #17547 ) ;
#31218=CARTESIAN_POINT ( 'NONE',  ( 0.000000000000000000, 2.755905511811024056, 0.000000000000000000 ) ) ;
#31255=CARTESIAN_POINT ( 'NONE',  ( -0.2834077913992259501, -0.6299212598425202314, -0.2440651625074179987 ) ) ;
#31258=VECTOR ( 'NONE', #8876, 39.37007874015748143 ) ;
#31402=DIRECTION ( 'NONE',  ( 0.000000000000000000, 1.000000000000000000, 0.000000000000000000 ) ) ;
#31533=DIRECTION ( 'NONE',  ( -0.000000000000000000, -1.000000000000000000, 0.000000000000000000 ) ) ;
#31550=ADVANCED_FACE ( 'NONE', ( #14667 ), #50228, .F. ) ;
#31665=VECTOR ( 'NONE', #553, 39.37007874015748143 ) ;
#31763=DIRECTION ( 'NONE',  ( 0.000000000000000000, -1.000000000000000000, 0.000000000000000000 ) ) ;
#31826=CARTESIAN_POINT ( 'NONE',  ( 0.000000000000000000, 7.874015748031496287, 0.000000000000000000 ) ) ;
#31871=EDGE_CURVE ( 'NONE', #2736, #14380, #8445, .T. ) ;
#31876=FACE_OUTER_BOUND ( 'NONE', #20462, .T. ) ;
#31913=ORIENTED_EDGE ( 'NONE', *, *, #14312, .T. ) ;
#32041=DIRECTION ( 'NONE',  ( -0.8268442224656336048, -0.000000000000000000, -0.5624310017906212211 ) ) ;
#32113=VERTEX_POINT ( 'NONE', #12997 ) ;
#32183=CARTESIAN_POINT ( 'NONE',  ( 0.000000000000000000, 0.000000000000000000, 0.000000000000000000 ) ) ;
#32393=ORIENTED_EDGE ( 'NONE', *, *, #32828, .T. ) ;
#32524=CARTESIAN_POINT ( 'NONE',  ( -0.06966273521059175577, -0.6299212598425202314, 0.3674709282358789575 ) ) ;
#32528=AXIS2_PLACEMENT_3D ( 'NONE', #27982, #20500, #36511 ) ;
#32533=ORIENTED_EDGE ( 'NONE', *, *, #30695, .F. ) ;
#32636=CARTESIAN_POINT ( 'NONE',  ( 0.000000000000000000, 2.755905511811024056, 0.000000000000000000 ) ) ;
#32741=AXIS2_PLACEMENT_3D ( 'NONE', #43015, #27528, #43270 ) ;
#32754=VECTOR ( 'NONE', #25350, 39.37007874015748143 ) ;
#32805=CARTESIAN_POINT ( 'NONE',  ( 1.039905234370930742, 0.000000000000000000, -0.5599999049406324536 ) ) ;
#32810=DIRECTION ( 'NONE',  ( -0.3166081466550566548, 0.000000000000000000, -0.9485564197619718030 ) ) ;
#32828=EDGE_CURVE ( 'NONE', #11586, #46126, #50524, .T. ) ;
#32836=VERTEX_POINT ( 'NONE', #17011 ) ;
#33030=ORIENTED_EDGE ( 'NONE', *, *, #24749, .T. ) ;
#33036=VECTOR ( 'NONE', #6327, 39.37007874015748143 ) ;
#33133=VERTEX_POINT ( 'NONE', #42770 ) ;
#33513=CIRCLE ( 'NONE', #43421, 1.181102362204723200 ) ;
#33596=EDGE_CURVE ( 'NONE', #48779, #43306, #41965, .T. ) ;
#33626=FACE_OUTER_BOUND ( 'NONE', #11467, .T. ) ;
#33738=ORIENTED_EDGE ( 'NONE', *, *, #50740, .T. ) ;
#33825=EDGE_LOOP ( 'NONE', ( #16714, #20789, #28339, #5716 ) ) ;
#33900=FACE_OUTER_BOUND ( 'NONE', #16793, .T. ) ;
#34025=VECTOR ( 'NONE', #28455, 39.37007874015748143 ) ;
#34246=CYLINDRICAL_SURFACE ( 'NONE', #720, 1.181102362204723200 ) ;
#34286=FACE_OUTER_BOUND ( 'NONE', #45071, .T. ) ;
#34429=SHAPE_REPRESENTATION ( 'Rotor', ( #26741 ), #43195 ) ;
#34432=ORIENTED_EDGE ( 'NONE', *, *, #8970, .F. ) ;
#34538=DIRECTION ( 'NONE',  ( -0.3166081466550567658, 0.000000000000000000, -0.9485564197619719140 ) ) ;
#34546=CARTESIAN_POINT ( 'NONE',  ( 0.000000000000000000, 2.755905511811024056, 0.000000000000000000 ) ) ;
#34588=DIRECTION ( 'NONE',  ( 0.000000000000000000, -1.000000000000000000, 0.000000000000000000 ) ) ;
#34699=ORIENTED_EDGE ( 'NONE', *, *, #8769, .F. ) ;
#34822=DIRECTION ( 'NONE',  ( -0.6631698831091616952, -0.000000000000000000, 0.7484689079293679326 ) ) ;
#34832=EDGE_CURVE ( 'NONE', #49027, #24066, #4897, .T. ) ;
#34934=AXIS2_PLACEMENT_3D ( 'NONE', #34546, #46132, #49474 ) ;
#34941=EDGE_LOOP ( 'NONE', ( #23754, #33030, #16635, #24093 ) ) ;
#34946=ORIENTED_EDGE ( 'NONE', *, *, #31871, .F. ) ;
#35128=FACE_OUTER_BOUND ( 'NONE', #1594, .T. ) ;
#35168=ORIENTED_EDGE ( 'NONE', *, *, #833, .T. ) ;
#35184=DIRECTION ( 'NONE',  ( 0.000000000000000000, 0.000000000000000000, -1.000000000000000000 ) ) ;
#35228=EDGE_CURVE ( 'NONE', #36716, #50620, #50353, .T. ) ;
#35253=DIRECTION ( 'NONE',  ( 0.000000000000000000, 1.000000000000000000, 0.000000000000000000 ) ) ;
#35257=ORIENTED_EDGE ( 'NONE', *, *, #12906, .T. ) ;
#35383=DIRECTION ( 'NONE',  ( -0.6631698831091616952, 0.000000000000000000, 0.7484689079293679326 ) ) ;
#35421=LINE ( 'NONE', #19903, #45111 ) ;
#35438=LINE ( 'NONE', #27673, #8439 ) ;
#35587=ORIENTED_EDGE ( 'NONE', *, *, #4555, .T. ) ;
#35611=ORIENTED_EDGE ( 'NONE', *, *, #11894, .F. ) ;
#35621=DIRECTION ( 'NONE',  ( -0.9465353838348410376, 0.000000000000000000, -0.3226000110797114240 ) ) ;
#35851=AXIS2_PLACEMENT_3D ( 'NONE', #22965, #38717, #41573 ) ;
#35884=ORIENTED_EDGE ( 'NONE', *, *, #14312, .F. ) ;
#35887=DIRECTION ( 'NONE',  ( 0.000000000000000000, 0.000000000000000000, -1.000000000000000000 ) ) ;
#35888=PLANE ( 'NONE',  #2585 ) ;
#35987=DIRECTION ( 'NONE',  ( 0.7526474967735860000, 0.000000000000000000, -0.6584236824419781309 ) ) ;
#36008=CARTESIAN_POINT ( 'NONE',  ( 0.000000000000000000, 0.000000000000000000, 0.000000000000000000 ) ) ;
#36070=DIRECTION ( 'NONE',  ( -0.07365742419378766559, 0.000000000000000000, 0.9972836025229415702 ) ) ;
#36163=DIRECTION ( 'NONE',  ( 0.000000000000000000, 1.000000000000000000, 0.000000000000000000 ) ) ;
#36180=DIRECTION ( 'NONE',  ( -0.8439299085898971375, 0.000000000000000000, 0.5364534550056020423 ) ) ;
#36229=DIRECTION ( 'NONE',  ( 1.000000000000000000, 0.000000000000000000, 0.000000000000000000 ) ) ;
#36329=DIRECTION ( 'NONE',  ( -0.8268442224656336048, 0.000000000000000000, -0.5624310017906212211 ) ) ;
#36409=ADVANCED_FACE ( 'NONE', ( #14071 ), #49895, .F. ) ;
#36470=FACE_OUTER_BOUND ( 'NONE', #20180, .T. ) ;
#36511=DIRECTION ( 'NONE',  ( -0.8660254037844362651, 0.000000000000000000, 0.5000000000000041078 ) ) ;
#36574=DIRECTION ( 'NONE',  ( 0.000000000000000000, -1.000000000000000000, 0.000000000000000000 ) ) ;
#36716=VERTEX_POINT ( 'NONE', #48314 ) ;
#36809=CARTESIAN_POINT ( 'NONE',  ( 0.000000000000000000, 2.755905511811024056, 0.000000000000000000 ) ) ;
#36899=VERTEX_POINT ( 'NONE', #46477 ) ;
#37053=ORIENTED_EDGE ( 'NONE', *, *, #24749, .F. ) ;
#37188=DIRECTION ( 'NONE',  ( -0.000000000000000000, -1.000000000000000000, 0.000000000000000000 ) ) ;
#37211=EDGE_LOOP ( 'NONE', ( #35257, #31913, #35611, #29649 ) ) ;
#37302=ORIENTED_EDGE ( 'NONE', *, *, #2595, .T. ) ;
#37564=DIRECTION ( 'NONE',  ( 0.000000000000000000, -1.000000000000000000, 0.000000000000000000 ) ) ;
#37568=VECTOR ( 'NONE', #516, 39.37007874015748143 ) ;
#37658=DIRECTION ( 'NONE',  ( 0.000000000000000000, -1.000000000000000000, 0.000000000000000000 ) ) ;
#37686=CIRCLE ( 'NONE', #15404, 1.181102362204723200 ) ;
#37735=CARTESIAN_POINT ( 'NONE',  ( 1.039905234370930520, 2.755905511811024056, -0.5599999049406324536 ) ) ;
#37788=VERTEX_POINT ( 'NONE', #15406 ) ;
#37820=CARTESIAN_POINT ( 'NONE',  ( 0.000000000000000000, 2.755905511811024056, 0.000000000000000000 ) ) ;
#37924=ADVANCED_FACE ( 'NONE', ( #3783 ), #47104, .F. ) ;
#37958=DIRECTION ( 'NONE',  ( 0.000000000000000000, -0.000000000000000000, 1.000000000000000000 ) ) ;
#37965=EDGE_CURVE ( 'NONE', #24641, #37788, #4549, .T. ) ;
#38022=CARTESIAN_POINT ( 'NONE',  ( 0.000000000000000000, 2.755905511811024056, -0.3740157480314960647 ) ) ;
#38172=CARTESIAN_POINT ( 'NONE',  ( 1.352759075253495258, -0.6299212598425202314, 0.2762566512555730269 ) ) ;
#38229=VECTOR ( 'NONE', #426, 39.37007874015748854 ) ;
#38254=DIRECTION ( 'NONE',  ( 0.9005016466594218949, -0.000000000000000000, -0.4348526007323282871 ) ) ;
#38288=CARTESIAN_POINT ( 'NONE',  ( 4.580371886574746102E-17, 2.755905511811024056, 0.3740157480314960647 ) ) ;
#38290=CARTESIAN_POINT ( 'NONE',  ( -0.06966273521059175577, 2.755905511811024056, 0.3674709282358789575 ) ) ;
#38322=CARTESIAN_POINT ( 'NONE',  ( -0.1692531782225912829, 2.755905511811024056, 0.3335283217915853138 ) ) ;
#38359=DIRECTION ( 'NONE',  ( 0.000000000000000000, -1.000000000000000000, 0.000000000000000000 ) ) ;
#38405=VECTOR ( 'NONE', #35253, 39.37007874015748143 ) ;
#38466=ORIENTED_EDGE ( 'NONE', *, *, #17339, .F. ) ;
#38499=ORIENTED_EDGE ( 'NONE', *, *, #7554, .T. ) ;
#38663=ORIENTED_EDGE ( 'NONE', *, *, #37965, .T. ) ;
#38717=DIRECTION ( 'NONE',  ( 0.000000000000000000, -1.000000000000000000, 0.000000000000000000 ) ) ;
#38799=FACE_OUTER_BOUND ( 'NONE', #48683, .T. ) ;
#38888=CARTESIAN_POINT ( 'NONE',  ( -0.2480359799030329715, 0.000000000000000000, 0.2799391584775194342 ) ) ;
#38982=FACE_OUTER_BOUND ( 'NONE', #4686, .T. ) ;
#39045=ORIENTED_EDGE ( 'NONE', *, *, #8838, .F. ) ;
#39242=LINE ( 'NONE', #31255, #37568 ) ;
#39243=DIRECTION ( 'NONE',  ( -0.9810236935216818388, 0.000000000000000000, 0.1938878870612536220 ) ) ;
#39308=ORIENTED_EDGE ( 'NONE', *, *, #37965, .F. ) ;
#39408=CARTESIAN_POINT ( 'NONE',  ( 0.3664524127070866721, 2.755905511811024056, 0.07483588040983164824 ) ) ;
#39416=CIRCLE ( 'NONE', #46821, 0.3740157480314960647 ) ;
#39560=DIRECTION ( 'NONE',  ( 0.8865472742777344983, 0.000000000000000000, 0.4626380123495249519 ) ) ;
#39644=CARTESIAN_POINT ( 'NONE',  ( -2.733043338785845690E-17, 0.000000000000000000, 1.338302322423841889E-16 ) ) ;
#39823=VERTEX_POINT ( 'NONE', #38290 ) ;
#39902=EDGE_CURVE ( 'NONE', #45331, #33133, #17990, .T. ) ;
#39936=CARTESIAN_POINT ( 'NONE',  ( 0.3699615006857430166, 0.000000000000000000, 0.02732463576302828281 ) ) ;
#40002=EDGE_CURVE ( 'NONE', #37788, #49027, #18316, .T. ) ;
#40007=PLANE ( 'NONE',  #1320 ) ;
#40029=PRODUCT_CONTEXT ( 'NONE', #49646, 'mechanical' ) ;
#40032=FACE_OUTER_BOUND ( 'NONE', #20843, .T. ) ;
#40082=DIRECTION ( 'NONE',  ( 0.9005016466594217839, 0.000000000000000000, -0.4348526007323282871 ) ) ;
#40108=PRODUCT ( 'Rotor', 'Rotor', '', ( #40029 ) ) ;
#40279=VECTOR ( 'NONE', #24403, 39.37007874015748143 ) ;
#40479=ORIENTED_EDGE ( 'NONE', *, *, #7554, .F. ) ;
#40486=DIRECTION ( 'NONE',  ( 0.000000000000000000, -1.000000000000000000, 0.000000000000000000 ) ) ;
#40545=LINE ( 'NONE', #12925, #6167 ) ;
#40624=DIRECTION ( 'NONE',  ( 0.000000000000000000, 0.000000000000000000, -1.000000000000000000 ) ) ;
#40637=ORIENTED_EDGE ( 'NONE', *, *, #39902, .T. ) ;
#40717=DIRECTION ( 'NONE',  ( -0.07365742419378766559, 0.000000000000000000, 0.9972836025229415702 ) ) ;
#40746=ORIENTED_EDGE ( 'NONE', *, *, #29827, .F. ) ;
#40767=CIRCLE ( 'NONE', #47307, 0.3740157480314961203 ) ;
#40805=CARTESIAN_POINT ( 'NONE',  ( 0.3664524127070866721, -0.6299212598425202314, 0.07483588040983164824 ) ) ;
#40867=VECTOR ( 'NONE', #8428, 39.37007874015748854 ) ;
#40932=CARTESIAN_POINT ( 'NONE',  ( -0.08518262569720812249, 0.000000000000000000, 0.003633560317753287746 ) ) ;
#40993=VERTEX_POINT ( 'NONE', #46232 ) ;
#41000=VERTEX_POINT ( 'NONE', #38022 ) ;
#41044=MANIFOLD_SOLID_BREP ( 'CirPattern1', #19652 ) ;
#41228=VERTEX_POINT ( 'NONE', #30204 ) ;
#41361=PLANE ( 'NONE',  #48000 ) ;
#41369=LENGTH_MEASURE_WITH_UNIT ( LENGTH_MEASURE( 0.02539999999999999897 ), #26126 );
#41449=DIRECTION ( 'NONE',  ( -0.4626380123495250074, 0.000000000000000000, 0.8865472742777346093 ) ) ;
#41540=CARTESIAN_POINT ( 'NONE',  ( -0.2834077913992259501, 2.755905511811024056, -0.2440651625074179987 ) ) ;
#41546=ORIENTED_EDGE ( 'NONE', *, *, #35228, .T. ) ;
#41573=DIRECTION ( 'NONE',  ( 0.000000000000000000, 0.000000000000000000, -1.000000000000000000 ) ) ;
#41624=SHAPE_REPRESENTATION_RELATIONSHIP ( 'NONE' , 'NONE' ,  #34429, #31011 ) ;
#41662=CARTESIAN_POINT ( 'NONE',  ( 0.000000000000000000, 2.755905511811024056, 0.000000000000000000 ) ) ;
#41691=CARTESIAN_POINT ( 'NONE',  ( -0.7832715154832613491, 2.755905511811024056, 0.8840183951921659622 ) ) ;
#41788=ORIENTED_EDGE ( 'NONE', *, *, #31871, .T. ) ;
#41799=CARTESIAN_POINT ( 'NONE',  ( 1.157218145390799258, 2.755905511811024056, 0.2363238328731523119 ) ) ;
#41806=VERTEX_POINT ( 'NONE', #26762 ) ;
#41839=CARTESIAN_POINT ( 'NONE',  ( -0.2086445790628121688, 0.000000000000000000, 0.3067337401345523462 ) ) ;
#41956=EDGE_CURVE ( 'NONE', #41000, #46126, #12159, .T. ) ;
#41965=LINE ( 'NONE', #6604, #17479 ) ;
#42026=DIRECTION ( 'NONE',  ( 0.000000000000000000, 0.000000000000000000, -1.000000000000000000 ) ) ;
#42030=FACE_OUTER_BOUND ( 'NONE', #48095, .T. ) ;
#42149=ADVANCED_FACE ( 'NONE', ( #45294 ), #9957, .F. ) ;
#42274=PLANE ( 'NONE',  #23948 ) ;
#42388=ADVANCED_FACE ( 'NONE', ( #20222 ), #16104, .F. ) ;
#42403=CARTESIAN_POINT ( 'NONE',  ( -0.2438126009205185685, 0.000000000000000000, -0.2787034377076138547 ) ) ;
#42550=DIRECTION ( 'NONE',  ( -0.9465353838348410376, 0.000000000000000000, -0.3226000110797114240 ) ) ;
#42562=EDGE_LOOP ( 'NONE', ( #9771, #48603, #41546, #9166, #3129, #6230, #45528, #16964, #20047, #41788, #27600, #14375, #33738, #35587, #12635, #3073 ) ) ;
#42593=EDGE_LOOP ( 'NONE', ( #6126, #12026, #19708, #38499 ) ) ;
#42626=FACE_OUTER_BOUND ( 'NONE', #27300, .T. ) ;
#42669=ORIENTED_EDGE ( 'NONE', *, *, #10105, .F. ) ;
#42770=CARTESIAN_POINT ( 'NONE',  ( -0.2042174104418111591, 2.755905511811024056, -0.3133417129078099328 ) ) ;
#42776=( GEOMETRIC_REPRESENTATION_CONTEXT ( 3 ) GLOBAL_UNCERTAINTY_ASSIGNED_CONTEXT ( ( #10198 ) ) GLOBAL_UNIT_ASSIGNED_CONTEXT ( ( #43383, #275, #15523 ) ) REPRESENTATION_CONTEXT ( 'NONE', 'WORKASPACE' ) );
#42895=ADVANCED_FACE ( 'NONE', ( #34286 ), #6148, .F. ) ;
#42959=EDGE_CURVE ( 'NONE', #46022, #23992, #46124, .T. ) ;
#43015=CARTESIAN_POINT ( 'NONE',  ( 0.000000000000000000, 2.755905511811024056, 0.000000000000000000 ) ) ;
#43065=ORIENTED_EDGE ( 'NONE', *, *, #10492, .T. ) ;
#43146=EDGE_CURVE ( 'NONE', #23992, #22341, #5650, .T. ) ;
#43195=( GEOMETRIC_REPRESENTATION_CONTEXT ( 3 ) GLOBAL_UNCERTAINTY_ASSIGNED_CONTEXT ( ( #24678 ) ) GLOBAL_UNIT_ASSIGNED_CONTEXT ( ( #5490, #48563, #48808 ) ) REPRESENTATION_CONTEXT ( 'NONE', 'WORKASPACE' ) );
#43270=DIRECTION ( 'NONE',  ( -0.8660254037844362651, 0.000000000000000000, 0.5000000000000039968 ) ) ;
#43306=VERTEX_POINT ( 'NONE', #1964 ) ;
#43383=( CONVERSION_BASED_UNIT ( 'INCH', #16029 ) LENGTH_UNIT ( ) NAMED_UNIT ( #11934 ) );
#43421=AXIS2_PLACEMENT_3D ( 'NONE', #31218, #34588, #11588 ) ;
#43533=CIRCLE ( 'NONE', #693, 0.3740157480314960647 ) ;
#43551=AXIS2_PLACEMENT_3D ( 'NONE', #21901, #37658, #26521 ) ;
#43624=EDGE_CURVE ( 'NONE', #40993, #16212, #16114, .T. ) ;
#43705=CARTESIAN_POINT ( 'NONE',  ( -0.2042174104418111591, -0.6299212598425202314, -0.3133417129078099328 ) ) ;
#43880=CARTESIAN_POINT ( 'NONE',  ( 0.000000000000000000, 7.874015748031496287, 0.000000000000000000 ) ) ;
#43939=ORIENTED_EDGE ( 'NONE', *, *, #40002, .F. ) ;
#44127=ORIENTED_EDGE ( 'NONE', *, *, #24686, .T. ) ;
#44146=CARTESIAN_POINT ( 'NONE',  ( 0.000000000000000000, 2.755905511811024056, 0.000000000000000000 ) ) ;
#44165=CARTESIAN_POINT ( 'NONE',  ( -0.06966273521059175577, -0.6299212598425202314, 0.3674709282358789575 ) ) ;
#44172=DIRECTION ( 'NONE',  ( 0.1938878870612535388, -0.000000000000000000, 0.9810236935216818388 ) ) ;
#44207=VECTOR ( 'NONE', #24681, 39.37007874015748143 ) ;
#44355=VECTOR ( 'NONE', #30792, 39.37007874015748143 ) ;
#44419=ADVANCED_FACE ( 'NONE', ( #38799 ), #22298, .T. ) ;
#44481=DIRECTION ( 'NONE',  ( 0.6584236824419781309, 0.000000000000000000, 0.7526474967735860000 ) ) ;
#44487=ORIENTED_EDGE ( 'NONE', *, *, #27278, .F. ) ;
#44548=ORIENTED_EDGE ( 'NONE', *, *, #17551, .F. ) ;
#44560=DIRECTION ( 'NONE',  ( 0.000000000000000000, 1.000000000000000000, 0.000000000000000000 ) ) ;
#44567=EDGE_CURVE ( 'NONE', #24292, #39823, #16579, .T. ) ;
#44661=CARTESIAN_POINT ( 'NONE',  ( 0.3734705886643994721, 2.755905511811024056, -0.02018660888377523527 ) ) ;
#44714=ORIENTED_EDGE ( 'NONE', *, *, #21064, .T. ) ;
#44783=EDGE_LOOP ( 'NONE', ( #27519, #23121, #6379, #20846 ) ) ;
#45002=PLANE ( 'NONE',  #2700 ) ;
#45008=AXIS2_PLACEMENT_3D ( 'NONE', #14526, #50336, #2901 ) ;
#45018=DIRECTION ( 'NONE',  ( -0.000000000000000000, -1.000000000000000000, 0.000000000000000000 ) ) ;
#45055=CARTESIAN_POINT ( 'NONE',  ( 0.000000000000000000, 7.874015748031496287, -0.3740157480314960647 ) ) ;
#45071=EDGE_LOOP ( 'NONE', ( #26960, #21327, #6579, #6377, #16198 ) ) ;
#45111=VECTOR ( 'NONE', #44172, 39.37007874015748143 ) ;
#45261=FACE_OUTER_BOUND ( 'NONE', #49124, .T. ) ;
#45294=FACE_OUTER_BOUND ( 'NONE', #34941, .T. ) ;
#45317=CYLINDRICAL_SURFACE ( 'NONE', #8662, 0.3740157480314960647 ) ;
#45331=VERTEX_POINT ( 'NONE', #41540 ) ;
#45347=CARTESIAN_POINT ( 'NONE',  ( 0.000000000000000000, 2.755905511811022723, 0.000000000000000000 ) ) ;
#45528=ORIENTED_EDGE ( 'NONE', *, *, #2021, .T. ) ;
#45536=CARTESIAN_POINT ( 'NONE',  ( -0.4371342596750092402, -0.6299212598425202314, -1.309652049997256373 ) ) ;
#45544=DIRECTION ( 'NONE',  ( 0.8865472742777344983, 0.000000000000000000, 0.4626380123495249519 ) ) ;
#45723=DIRECTION ( 'NONE',  ( 0.000000000000000000, 0.000000000000000000, -1.000000000000000000 ) ) ;
#45787=LINE ( 'NONE', #41691, #33036 ) ;
#45813=CIRCLE ( 'NONE', #49918, 1.181102362204723200 ) ;
#45853=AXIS2_PLACEMENT_3D ( 'NONE', #48859, #45018, #29545 ) ;
#45898=ORIENTED_EDGE ( 'NONE', *, *, #32828, .F. ) ;
#46022=VERTEX_POINT ( 'NONE', #30999 ) ;
#46045=STYLED_ITEM('',(#51101),#41044);
#46124=LINE ( 'NONE', #18783, #16372 ) ;
#46126=VERTEX_POINT ( 'NONE', #30496 ) ;
#46132=DIRECTION ( 'NONE',  ( 0.000000000000000000, -1.000000000000000000, 0.000000000000000000 ) ) ;
#46186=ADVANCED_FACE ( 'NONE', ( #517 ), #35888, .F. ) ;
#46232=CARTESIAN_POINT ( 'NONE',  ( 4.580371886574746102E-17, 7.874015748031496287, 0.3740157480314960647 ) ) ;
#46477=CARTESIAN_POINT ( 'NONE',  ( 0.000000000000000000, 2.755905511811024056, -1.181102362204723200 ) ) ;
#46510=CIRCLE ( 'NONE', #16885, 1.181102362204723200 ) ;
#46624=CARTESIAN_POINT ( 'NONE',  ( 0.000000000000000000, 2.755905511811024056, 0.000000000000000000 ) ) ;
#46721=DIRECTION ( 'NONE',  ( 0.000000000000000000, -1.000000000000000000, 0.000000000000000000 ) ) ;
#46738=EDGE_LOOP ( 'NONE', ( #9547, #40479, #44714, #2391, #45898, #16873 ) ) ;
#46821=AXIS2_PLACEMENT_3D ( 'NONE', #17530, #49486, #2293 ) ;
#46887=ORIENTED_EDGE ( 'NONE', *, *, #24287, .F. ) ;
#46952=DIRECTION ( 'NONE',  ( 0.000000000000000000, 1.000000000000000000, 0.000000000000000000 ) ) ;
#47029=DIRECTION ( 'NONE',  ( 0.000000000000000000, -1.000000000000000000, 0.000000000000000000 ) ) ;
#47104=PLANE ( 'NONE',  #12402 ) ;
#47276=DIRECTION ( 'NONE',  ( -0.6631698831091616952, 0.000000000000000000, 0.7484689079293679326 ) ) ;
#47307=AXIS2_PLACEMENT_3D ( 'NONE', #46624, #3286, #23406 ) ;
#47423=ORIENTED_EDGE ( 'NONE', *, *, #8769, .T. ) ;
#47481=ORIENTED_EDGE ( 'NONE', *, *, #14249, .T. ) ;
#47572=EDGE_LOOP ( 'NONE', ( #4085, #16914 ) ) ;
#47602=EDGE_CURVE ( 'NONE', #945, #11586, #12983, .T. ) ;
#47621=DIRECTION ( 'NONE',  ( -0.000000000000000000, 1.000000000000000000, -0.000000000000000000 ) ) ;
#47794=ORIENTED_EDGE ( 'NONE', *, *, #47602, .T. ) ;
#47884=DIRECTION ( 'NONE',  ( 0.000000000000000000, 0.000000000000000000, -1.000000000000000000 ) ) ;
#47906=EDGE_LOOP ( 'NONE', ( #43065, #30704, #34699, #34946 ) ) ;
#47931=AXIS2_PLACEMENT_3D ( 'NONE', #22502, #10378, #25608 ) ;
#47944=DIRECTION ( 'NONE',  ( -0.8439299085898971375, -0.000000000000000000, 0.5364534550056020423 ) ) ;
#47946=LINE ( 'NONE', #28871, #28399 ) ;
#47947=EDGE_CURVE ( 'NONE', #39823, #286, #1875, .T. ) ;
#48000=AXIS2_PLACEMENT_3D ( 'NONE', #13483, #21740, #13235 ) ;
#48002=PLANE ( 'NONE',  #30009 ) ;
#48095=EDGE_LOOP ( 'NONE', ( #17909, #37, #47423, #47481 ) ) ;
#48114=ORIENTED_EDGE ( 'NONE', *, *, #30239, .F. ) ;
#48207=AXIS2_PLACEMENT_3D ( 'NONE', #5592, #48404, #36329 ) ;
#48275=AXIS2_PLACEMENT_3D ( 'NONE', #17476, #21100, #40717 ) ;
#48314=CARTESIAN_POINT ( 'NONE',  ( -0.2834077913992260056, 0.000000000000000000, -0.2440651625074179987 ) ) ;
#48404=DIRECTION ( 'NONE',  ( 0.5624310017906212211, 0.000000000000000000, -0.8268442224656336048 ) ) ;
#48436=DIRECTION ( 'NONE',  ( 0.000000000000000000, 0.000000000000000000, -1.000000000000000000 ) ) ;
#48563=( NAMED_UNIT ( * ) PLANE_ANGLE_UNIT ( ) SI_UNIT ( $, .RADIAN. ) );
#48603=ORIENTED_EDGE ( 'NONE', *, *, #48615, .T. ) ;
#48615=EDGE_CURVE ( 'NONE', #32836, #36716, #35438, .T. ) ;
#48683=EDGE_LOOP ( 'NONE', ( #5410, #25586, #832, #13691 ) ) ;
#48779=VERTEX_POINT ( 'NONE', #41799 ) ;
#48808=( NAMED_UNIT ( * ) SI_UNIT ( $, .STERADIAN. ) SOLID_ANGLE_UNIT ( ) );
#48859=CARTESIAN_POINT ( 'NONE',  ( 0.000000000000000000, 2.755905511811022723, 0.000000000000000000 ) ) ;
#48942=DIRECTION ( 'NONE',  ( 0.8660254037844431485, 0.000000000000000000, 0.4999999999999918954 ) ) ;
#49027=VERTEX_POINT ( 'NONE', #50998 ) ;
#49124=EDGE_LOOP ( 'NONE', ( #14982, #44487 ) ) ;
#49130=CYLINDRICAL_SURFACE ( 'NONE', #8396, 1.181102362204723200 ) ;
#49421=VECTOR ( 'NONE', #11931, 39.37007874015748854 ) ;
#49432=FACE_OUTER_BOUND ( 'NONE', #6820, .T. ) ;
#49474=DIRECTION ( 'NONE',  ( 0.000000000000000000, -0.000000000000000000, -1.000000000000000000 ) ) ;
#49486=DIRECTION ( 'NONE',  ( 0.000000000000000000, -1.000000000000000000, 0.000000000000000000 ) ) ;
#49646=APPLICATION_CONTEXT ( 'automotive_design' ) ;
#49765=LINE ( 'NONE', #14454, #18393 ) ;
#49778=VECTOR ( 'NONE', #36070, 39.37007874015748854 ) ;
#49878=EDGE_CURVE ( 'NONE', #24641, #10066, #24594, .T. ) ;
#49895=PLANE ( 'NONE',  #24659 ) ;
#49901=CARTESIAN_POINT ( 'NONE',  ( 0.000000000000000000, 0.000000000000000000, -1.181102362204723200 ) ) ;
#49918=AXIS2_PLACEMENT_3D ( 'NONE', #12094, #40486, #48436 ) ;
#49950=ORIENTED_EDGE ( 'NONE', *, *, #43624, .T. ) ;
#49965=ORIENTED_EDGE ( 'NONE', *, *, #12871, .F. ) ;
#49978=ADVANCED_FACE ( 'NONE', ( #33626 ), #41361, .T. ) ;
#50042=AXIS2_PLACEMENT_3D ( 'NONE', #43705, #44481, #35987 ) ;
#50068=CARTESIAN_POINT ( 'NONE',  ( 0.000000000000000000, 7.874015748031496287, 0.000000000000000000 ) ) ;
#50208=CARTESIAN_POINT ( 'NONE',  ( -0.1184164328040565317, 2.755905511811024056, -0.3547750388873516791 ) ) ;
#50228=PLANE ( 'NONE',  #34934 ) ;
#50238=CARTESIAN_POINT ( 'NONE',  ( 0.3734705886643994721, 0.000000000000000000, -0.02018660888377523527 ) ) ;
#50286=DIRECTION ( 'NONE',  ( -0.8268442224656336048, 0.000000000000000000, -0.5624310017906212211 ) ) ;
#50306=PLANE ( 'NONE',  #21902 ) ;
#50336=DIRECTION ( 'NONE',  ( -0.5364534550056021533, 0.000000000000000000, -0.8439299085898972486 ) ) ;
#50353=LINE ( 'NONE', #42403, #44355 ) ;
#50478=CARTESIAN_POINT ( 'NONE',  ( -0.1184164328040565317, -0.6299212598425202314, -0.3547750388873516791 ) ) ;
#50524=LINE ( 'NONE', #4113, #14449 ) ;
#50620=VERTEX_POINT ( 'NONE', #21054 ) ;
#50660=EDGE_CURVE ( 'NONE', #14380, #43306, #28792, .T. ) ;
#50675=AXIS2_PLACEMENT_3D ( 'NONE', #4137, #31763, #35887 ) ;
#50700=FACE_OUTER_BOUND ( 'NONE', #47572, .T. ) ;
#50740=EDGE_CURVE ( 'NONE', #1528, #13306, #6063, .T. ) ;
#50835=LINE ( 'NONE', #20421, #31665 ) ;
#50892=ORIENTED_EDGE ( 'NONE', *, *, #41956, .F. ) ;
#50901=VECTOR ( 'NONE', #34822, 39.37007874015748854 ) ;
#50998=CARTESIAN_POINT ( 'NONE',  ( -0.7832715154832613491, 2.755905511811024056, 0.8840183951921660732 ) ) ;
#51095=COLOUR_RGB('Off White',0.89,0.88,0.83);
#51096=FILL_AREA_STYLE_COLOUR('',#51095);
#51097=FILL_AREA_STYLE('',(#51096));
#51098=SURFACE_STYLE_FILL_AREA(#51097);
#51099=SURFACE_SIDE_STYLE('',(#51098));
#51100=SURFACE_STYLE_USAGE(.BOTH.,#51099);
#51101=PRESENTATION_STYLE_ASSIGNMENT((#51100));
ENDSEC;
END-ISO-10303-21;
